ISO-10303-21;
HEADER;
/* Generated by software containing ST-Developer
 * from STEP Tools, Inc. (www.steptools.com) 
 */

FILE_DESCRIPTION(
/* description */ ('Door-style hinge test fixture with detent'),
/* implementation_level */ '2;1');

FILE_NAME(
/* name */ 'Flat Washer - M6.step',
/* time_stamp */ '2026-10-28T03:24:57-07:00',
/* author */ (''),
/* organization */ (''),
/* preprocessor_version */ 'ST-DEVELOPER v20.2',
/* originating_system */ 'Autodesk Translation Framework v15.17.0.0',
/* authorisation */ '');

FILE_SCHEMA (('AUTOMOTIVE_DESIGN { 1 0 10303 214 3 1 1 }'));
ENDSEC;

DATA;
#10=MECHANICAL_DESIGN_GEOMETRIC_PRESENTATION_REPRESENTATION('',(#340),#9813);
#277=SHAPE_REPRESENTATION_RELATIONSHIP('SRR','None',#9954,#308);
#308=ADVANCED_BREP_SHAPE_REPRESENTATION('',(#380),#9797);
#340=STYLED_ITEM('',(#10190),#380);
#380=MANIFOLD_SOLID_BREP('Body1',#4771);
#465=FACE_BOUND('',#1159,.T.);
#466=FACE_BOUND('',#1161,.T.);
#592=PLANE('',#5416);
#593=PLANE('',#5417);
#805=FACE_OUTER_BOUND('',#1156,.T.);
#806=FACE_OUTER_BOUND('',#1157,.T.);
#807=FACE_OUTER_BOUND('',#1158,.T.);
#808=FACE_OUTER_BOUND('',#1160,.T.);
#1156=EDGE_LOOP('',(#3827,#3828,#3829,#3830));
#1157=EDGE_LOOP('',(#3831,#3832,#3833,#3834));
#1158=EDGE_LOOP('',(#3835));
#1159=EDGE_LOOP('',(#3836));
#1160=EDGE_LOOP('',(#3837));
#1161=EDGE_LOOP('',(#3838));
#1532=LINE('',#8694,#1852);
#1533=LINE('',#8700,#1853);
#1852=VECTOR('',#6497,0.32);
#1853=VECTOR('',#6504,0.6);
#2085=CIRCLE('',#5411,0.32);
#2086=CIRCLE('',#5412,0.32);
#2087=CIRCLE('',#5414,0.6);
#2088=CIRCLE('',#5415,0.6);
#2429=VERTEX_POINT('',#8691);
#2430=VERTEX_POINT('',#8693);
#2431=VERTEX_POINT('',#8697);
#2432=VERTEX_POINT('',#8699);
#2930=EDGE_CURVE('',#2429,#2429,#2085,.T.);
#2931=EDGE_CURVE('',#2429,#2430,#1532,.T.);
#2932=EDGE_CURVE('',#2430,#2430,#2086,.T.);
#2933=EDGE_CURVE('',#2431,#2431,#2087,.T.);
#2934=EDGE_CURVE('',#2431,#2432,#1533,.T.);
#2935=EDGE_CURVE('',#2432,#2432,#2088,.T.);
#3827=ORIENTED_EDGE('',*,*,#2930,.F.);
#3828=ORIENTED_EDGE('',*,*,#2931,.T.);
#3829=ORIENTED_EDGE('',*,*,#2932,.T.);
#3830=ORIENTED_EDGE('',*,*,#2931,.F.);
#3831=ORIENTED_EDGE('',*,*,#2933,.F.);
#3832=ORIENTED_EDGE('',*,*,#2934,.T.);
#3833=ORIENTED_EDGE('',*,*,#2935,.T.);
#3834=ORIENTED_EDGE('',*,*,#2934,.F.);
#3835=ORIENTED_EDGE('',*,*,#2933,.T.);
#3836=ORIENTED_EDGE('',*,*,#2930,.T.);
#3837=ORIENTED_EDGE('',*,*,#2935,.F.);
#3838=ORIENTED_EDGE('',*,*,#2932,.F.);
#4429=CYLINDRICAL_SURFACE('',#5410,0.32);
#4430=CYLINDRICAL_SURFACE('',#5413,0.6);
#4610=ADVANCED_FACE('',(#805),#4429,.F.);
#4611=ADVANCED_FACE('',(#806),#4430,.T.);
#4612=ADVANCED_FACE('',(#807,#465),#592,.T.);
#4613=ADVANCED_FACE('',(#808,#466),#593,.F.);
#4771=CLOSED_SHELL('',(#4610,#4611,#4612,#4613));
#5409=AXIS2_PLACEMENT_3D('',#8689,#6491,#6492);
#5410=AXIS2_PLACEMENT_3D('',#8690,#6493,#6494);
#5411=AXIS2_PLACEMENT_3D('',#8692,#6495,#6496);
#5412=AXIS2_PLACEMENT_3D('',#8695,#6498,#6499);
#5413=AXIS2_PLACEMENT_3D('',#8696,#6500,#6501);
#5414=AXIS2_PLACEMENT_3D('',#8698,#6502,#6503);
#5415=AXIS2_PLACEMENT_3D('',#8701,#6505,#6506);
#5416=AXIS2_PLACEMENT_3D('',#8702,#6507,#6508);
#5417=AXIS2_PLACEMENT_3D('',#8703,#6509,#6510);
#6491=DIRECTION('axis',(0.,0.,1.));
#6492=DIRECTION('refdir',(1.,0.,0.));
#6493=DIRECTION('center_axis',(0.,1.,0.));
#6494=DIRECTION('ref_axis',(1.,0.,0.));
#6495=DIRECTION('center_axis',(0.,-1.,0.));
#6496=DIRECTION('ref_axis',(1.,0.,0.));
#6497=DIRECTION('',(0.,-1.,0.));
#6498=DIRECTION('center_axis',(0.,-1.,0.));
#6499=DIRECTION('ref_axis',(1.,0.,0.));
#6500=DIRECTION('center_axis',(0.,1.,0.));
#6501=DIRECTION('ref_axis',(1.,0.,0.));
#6502=DIRECTION('center_axis',(0.,1.,0.));
#6503=DIRECTION('ref_axis',(1.,0.,0.));
#6504=DIRECTION('',(0.,-1.,0.));
#6505=DIRECTION('center_axis',(0.,1.,0.));
#6506=DIRECTION('ref_axis',(1.,0.,0.));
#6507=DIRECTION('center_axis',(0.,1.,0.));
#6508=DIRECTION('ref_axis',(1.,0.,0.));
#6509=DIRECTION('center_axis',(0.,1.,0.));
#6510=DIRECTION('ref_axis',(1.,0.,0.));
#8689=CARTESIAN_POINT('',(0.,0.,0.));
#8690=CARTESIAN_POINT('Origin',(0.,0.,0.));
#8691=CARTESIAN_POINT('',(-0.32,0.16,3.91886975727153E-17));
#8692=CARTESIAN_POINT('Origin',(0.,0.16,0.));
#8693=CARTESIAN_POINT('',(-0.32,0.,3.91886975727153E-17));
#8694=CARTESIAN_POINT('',(-0.32,0.,3.91886975727153E-17));
#8695=CARTESIAN_POINT('Origin',(0.,0.,0.));
#8696=CARTESIAN_POINT('Origin',(0.,0.,0.));
#8697=CARTESIAN_POINT('',(-0.6,0.16,7.34788079488412E-17));
#8698=CARTESIAN_POINT('Origin',(0.,0.16,0.));
#8699=CARTESIAN_POINT('',(-0.6,0.,7.34788079488412E-17));
#8700=CARTESIAN_POINT('',(-0.6,0.,7.34788079488412E-17));
#8701=CARTESIAN_POINT('Origin',(0.,0.,0.));
#8702=CARTESIAN_POINT('Origin',(0.,0.16,0.));
#8703=CARTESIAN_POINT('Origin',(0.,0.,0.));
#9761=UNCERTAINTY_MEASURE_WITH_UNIT(LENGTH_MEASURE(0.001),#9814,
'DISTANCE_ACCURACY_VALUE',
'Maximum model space distance between geometric entities at asserted c
onnectivities');
#9777=UNCERTAINTY_MEASURE_WITH_UNIT(LENGTH_MEASURE(0.001),#9814,
'DISTANCE_ACCURACY_VALUE',
'Maximum model space distance between geometric entities at asserted c
onnectivities');
#9797=(
GEOMETRIC_REPRESENTATION_CONTEXT(3)
GLOBAL_UNCERTAINTY_ASSIGNED_CONTEXT((#9761))
GLOBAL_UNIT_ASSIGNED_CONTEXT((#9814,#9816,#9817))
REPRESENTATION_CONTEXT('','3D')
);
#9813=(
GEOMETRIC_REPRESENTATION_CONTEXT(3)
GLOBAL_UNCERTAINTY_ASSIGNED_CONTEXT((#9777))
GLOBAL_UNIT_ASSIGNED_CONTEXT((#9814,#9816,#9817))
REPRESENTATION_CONTEXT('','3D')
);
#9814=(
LENGTH_UNIT()
NAMED_UNIT(*)
SI_UNIT(.CENTI.,.METRE.)
);
#9816=(
NAMED_UNIT(*)
PLANE_ANGLE_UNIT()
SI_UNIT($,.RADIAN.)
);
#9817=(
NAMED_UNIT(*)
SI_UNIT($,.STERADIAN.)
SOLID_ANGLE_UNIT()
);
#9837=SHAPE_DEFINITION_REPRESENTATION(#9872,#9954);
#9872=PRODUCT_DEFINITION_SHAPE('',$,#9990);
#9954=SHAPE_REPRESENTATION('',(#5409),#9797);
#9970=PRODUCT_DEFINITION_CONTEXT('part definition',#10077,'design');
#9990=PRODUCT_DEFINITION('Flat Washer - M6','Flat Washer - M6',#10025,#9970);
#10025=PRODUCT_DEFINITION_FORMATION('',$,#10098);
#10077=APPLICATION_CONTEXT(
'Core Data for Automotive Mechanical Design Process');
#10078=PRODUCT_CONTEXT('part definition',#10077,'mechanical');
#10098=PRODUCT('Flat Washer - M6','Flat Washer - M6','Flat Washer - M6',
(#10078));
#10184=COLOUR_RGB('Black',0.12,0.14,0.17);
#10185=FILL_AREA_STYLE_COLOUR('',#10184);
#10186=FILL_AREA_STYLE('',(#10185));
#10187=SURFACE_STYLE_FILL_AREA(#10186);
#10188=SURFACE_SIDE_STYLE('',(#10187));
#10189=SURFACE_STYLE_USAGE(.BOTH.,#10188);
#10190=PRESENTATION_STYLE_ASSIGNMENT((#10189));
ENDSEC;
END-ISO-10303-21;
